ISO-10303-21;
HEADER;
/* Generated by software containing ST-Developer
 * from STEP Tools, Inc. (www.steptools.com) 
 */

FILE_DESCRIPTION(
/* description */ ('Cable chain and bracket set'),
/* implementation_level */ '2;1');

FILE_NAME(
/* name */ 'Forty millimetre hinge bolt__PD6069.step',
/* time_stamp */ '2026-10-29T17:19:47-07:00',
/* author */ (''),
/* organization */ (''),
/* preprocessor_version */ 'ST-DEVELOPER v20.2',
/* originating_system */ 'Autodesk Translation Framework v15.17.0.0',
/* authorisation */ '');

FILE_SCHEMA (('AUTOMOTIVE_DESIGN { 1 0 10303 214 3 1 1 }'));
ENDSEC;

DATA;
#10=MECHANICAL_DESIGN_GEOMETRIC_PRESENTATION_REPRESENTATION('',(#340),#5929);
#247=(
BOUNDED_CURVE()
B_SPLINE_CURVE(2,(#5191,#5192,#5193),.UNSPECIFIED.,.F.,.F.)
B_SPLINE_CURVE_WITH_KNOTS((3,3),(0.144988513094728,0.791574906712449),
 .UNSPECIFIED.)
CURVE()
GEOMETRIC_REPRESENTATION_ITEM()
RATIONAL_B_SPLINE_CURVE((1.09282032302755,1.26188021535082,1.09282032302931))
REPRESENTATION_ITEM('')
);
#248=(
BOUNDED_CURVE()
B_SPLINE_CURVE(2,(#5195,#5196,#5197),.UNSPECIFIED.,.F.,.F.)
B_SPLINE_CURVE_WITH_KNOTS((3,3),(0.144988513094728,0.791574906712449),
 .UNSPECIFIED.)
CURVE()
GEOMETRIC_REPRESENTATION_ITEM()
RATIONAL_B_SPLINE_CURVE((1.09282032302755,1.26188021535082,1.09282032302931))
REPRESENTATION_ITEM('')
);
#249=(
BOUNDED_CURVE()
B_SPLINE_CURVE(2,(#5199,#5200,#5201),.UNSPECIFIED.,.F.,.F.)
B_SPLINE_CURVE_WITH_KNOTS((3,3),(0.144988513094728,0.791574906712449),
 .UNSPECIFIED.)
CURVE()
GEOMETRIC_REPRESENTATION_ITEM()
RATIONAL_B_SPLINE_CURVE((1.09282032302755,1.26188021535082,1.09282032302931))
REPRESENTATION_ITEM('')
);
#250=(
BOUNDED_CURVE()
B_SPLINE_CURVE(2,(#5203,#5204,#5205),.UNSPECIFIED.,.F.,.F.)
B_SPLINE_CURVE_WITH_KNOTS((3,3),(0.144988513094728,0.791574906712449),
 .UNSPECIFIED.)
CURVE()
GEOMETRIC_REPRESENTATION_ITEM()
RATIONAL_B_SPLINE_CURVE((1.09282032302755,1.26188021535082,1.09282032302931))
REPRESENTATION_ITEM('')
);
#251=(
BOUNDED_CURVE()
B_SPLINE_CURVE(2,(#5207,#5208,#5209),.UNSPECIFIED.,.F.,.F.)
B_SPLINE_CURVE_WITH_KNOTS((3,3),(0.144988513094728,0.791574906712449),
 .UNSPECIFIED.)
CURVE()
GEOMETRIC_REPRESENTATION_ITEM()
RATIONAL_B_SPLINE_CURVE((1.09282032302755,1.26188021535082,1.09282032302931))
REPRESENTATION_ITEM('')
);
#252=(
BOUNDED_CURVE()
B_SPLINE_CURVE(2,(#5210,#5211,#5212),.UNSPECIFIED.,.F.,.F.)
B_SPLINE_CURVE_WITH_KNOTS((3,3),(0.144988513094727,0.791574906712449),
 .UNSPECIFIED.)
CURVE()
GEOMETRIC_REPRESENTATION_ITEM()
RATIONAL_B_SPLINE_CURVE((1.09282032302755,1.26188021535082,1.09282032302931))
REPRESENTATION_ITEM('')
);
#283=CONICAL_SURFACE('',#3546,0.270000000000031,0.785398163397448);
#284=CONICAL_SURFACE('',#3547,0.576175134594879,1.0471975511966);
#314=SHAPE_REPRESENTATION_RELATIONSHIP('SRR','None',#6045,#327);
#327=ADVANCED_BREP_SHAPE_REPRESENTATION('',(#353),#5912);
#340=STYLED_ITEM('',(#6227),#353);
#353=MANIFOLD_SOLID_BREP('Body1',#3334);
#377=FACE_BOUND('',#784,.T.);
#378=FACE_BOUND('',#798,.T.);
#445=PLANE('',#3537);
#446=PLANE('',#3542);
#447=PLANE('',#3549);
#448=PLANE('',#3550);
#449=PLANE('',#3551);
#450=PLANE('',#3552);
#451=PLANE('',#3553);
#452=PLANE('',#3554);
#453=PLANE('',#3555);
#454=PLANE('',#3556);
#587=FACE_OUTER_BOUND('',#783,.T.);
#588=FACE_OUTER_BOUND('',#785,.T.);
#589=FACE_OUTER_BOUND('',#786,.T.);
#590=FACE_OUTER_BOUND('',#787,.T.);
#591=FACE_OUTER_BOUND('',#788,.T.);
#592=FACE_OUTER_BOUND('',#789,.T.);
#593=FACE_OUTER_BOUND('',#790,.T.);
#594=FACE_OUTER_BOUND('',#791,.T.);
#595=FACE_OUTER_BOUND('',#792,.T.);
#596=FACE_OUTER_BOUND('',#793,.T.);
#597=FACE_OUTER_BOUND('',#794,.T.);
#598=FACE_OUTER_BOUND('',#795,.T.);
#599=FACE_OUTER_BOUND('',#796,.T.);
#600=FACE_OUTER_BOUND('',#797,.T.);
#783=EDGE_LOOP('',(#2549));
#784=EDGE_LOOP('',(#2550));
#785=EDGE_LOOP('',(#2551,#2552,#2553,#2554));
#786=EDGE_LOOP('',(#2555));
#787=EDGE_LOOP('',(#2556,#2557,#2558,#2559));
#788=EDGE_LOOP('',(#2560,#2561,#2562,#2563));
#789=EDGE_LOOP('',(#2564,#2565,#2566,#2567,#2568,#2569,#2570,#2571,#2572));
#790=EDGE_LOOP('',(#2573,#2574,#2575,#2576));
#791=EDGE_LOOP('',(#2577,#2578,#2579,#2580));
#792=EDGE_LOOP('',(#2581,#2582,#2583,#2584));
#793=EDGE_LOOP('',(#2585,#2586,#2587,#2588));
#794=EDGE_LOOP('',(#2589,#2590,#2591,#2592));
#795=EDGE_LOOP('',(#2593,#2594,#2595,#2596));
#796=EDGE_LOOP('',(#2597));
#797=EDGE_LOOP('',(#2598,#2599,#2600,#2601,#2602,#2603));
#798=EDGE_LOOP('',(#2604));
#1035=LINE('',#5174,#1295);
#1036=LINE('',#5181,#1296);
#1037=LINE('',#5184,#1297);
#1038=LINE('',#5189,#1298);
#1039=LINE('',#5215,#1299);
#1040=LINE('',#5217,#1300);
#1041=LINE('',#5218,#1301);
#1042=LINE('',#5221,#1302);
#1043=LINE('',#5222,#1303);
#1044=LINE('',#5225,#1304);
#1045=LINE('',#5226,#1305);
#1046=LINE('',#5229,#1306);
#1047=LINE('',#5230,#1307);
#1048=LINE('',#5233,#1308);
#1049=LINE('',#5234,#1309);
#1050=LINE('',#5236,#1310);
#1295=VECTOR('',#4154,0.300000000000034);
#1296=VECTOR('',#4163,0.300000000000034);
#1297=VECTOR('',#4168,0.270000000000031);
#1298=VECTOR('',#4173,0.576175134594879);
#1299=VECTOR('',#4176,1.00000000000011);
#1300=VECTOR('',#4177,1.00000000000011);
#1301=VECTOR('',#4178,1.00000000000011);
#1302=VECTOR('',#4181,1.00000000000011);
#1303=VECTOR('',#4182,1.00000000000011);
#1304=VECTOR('',#4185,1.00000000000011);
#1305=VECTOR('',#4186,1.00000000000011);
#1306=VECTOR('',#4189,1.00000000000011);
#1307=VECTOR('',#4190,1.00000000000011);
#1308=VECTOR('',#4193,1.00000000000011);
#1309=VECTOR('',#4194,1.00000000000011);
#1310=VECTOR('',#4197,1.00000000000011);
#1491=CIRCLE('',#3538,0.300000000000034);
#1492=CIRCLE('',#3539,0.250000000000028);
#1493=CIRCLE('',#3541,0.300000000000034);
#1494=CIRCLE('',#3544,0.294200000000034);
#1495=CIRCLE('',#3545,0.294200000000034);
#1496=CIRCLE('',#3548,0.475000000000054);
#1653=VERTEX_POINT('',#5168);
#1654=VERTEX_POINT('',#5170);
#1655=VERTEX_POINT('',#5173);
#1656=VERTEX_POINT('',#5178);
#1657=VERTEX_POINT('',#5180);
#1658=VERTEX_POINT('',#5186);
#1659=VERTEX_POINT('',#5188);
#1660=VERTEX_POINT('',#5190);
#1661=VERTEX_POINT('',#5194);
#1662=VERTEX_POINT('',#5198);
#1663=VERTEX_POINT('',#5202);
#1664=VERTEX_POINT('',#5206);
#1665=VERTEX_POINT('',#5214);
#1666=VERTEX_POINT('',#5216);
#1667=VERTEX_POINT('',#5220);
#1668=VERTEX_POINT('',#5224);
#1669=VERTEX_POINT('',#5228);
#1670=VERTEX_POINT('',#5232);
#1975=EDGE_CURVE('',#1653,#1653,#1491,.T.);
#1976=EDGE_CURVE('',#1654,#1654,#1492,.T.);
#1977=EDGE_CURVE('',#1653,#1655,#1035,.T.);
#1978=EDGE_CURVE('',#1655,#1655,#1493,.T.);
#1979=EDGE_CURVE('',#1656,#1656,#1494,.F.);
#1980=EDGE_CURVE('',#1656,#1657,#1036,.T.);
#1981=EDGE_CURVE('',#1657,#1657,#1495,.F.);
#1982=EDGE_CURVE('',#1654,#1656,#1037,.T.);
#1983=EDGE_CURVE('',#1658,#1658,#1496,.T.);
#1984=EDGE_CURVE('',#1658,#1659,#1038,.T.);
#1985=EDGE_CURVE('',#1660,#1659,#247,.T.);
#1986=EDGE_CURVE('',#1661,#1660,#248,.T.);
#1987=EDGE_CURVE('',#1662,#1661,#249,.T.);
#1988=EDGE_CURVE('',#1663,#1662,#250,.T.);
#1989=EDGE_CURVE('',#1664,#1663,#251,.T.);
#1990=EDGE_CURVE('',#1659,#1664,#252,.T.);
#1991=EDGE_CURVE('',#1665,#1663,#1039,.T.);
#1992=EDGE_CURVE('',#1665,#1666,#1040,.T.);
#1993=EDGE_CURVE('',#1666,#1664,#1041,.T.);
#1994=EDGE_CURVE('',#1667,#1662,#1042,.T.);
#1995=EDGE_CURVE('',#1667,#1665,#1043,.T.);
#1996=EDGE_CURVE('',#1668,#1661,#1044,.T.);
#1997=EDGE_CURVE('',#1668,#1667,#1045,.T.);
#1998=EDGE_CURVE('',#1669,#1660,#1046,.T.);
#1999=EDGE_CURVE('',#1669,#1668,#1047,.T.);
#2000=EDGE_CURVE('',#1670,#1659,#1048,.T.);
#2001=EDGE_CURVE('',#1670,#1669,#1049,.T.);
#2002=EDGE_CURVE('',#1666,#1670,#1050,.T.);
#2549=ORIENTED_EDGE('',*,*,#1975,.T.);
#2550=ORIENTED_EDGE('',*,*,#1976,.F.);
#2551=ORIENTED_EDGE('',*,*,#1975,.F.);
#2552=ORIENTED_EDGE('',*,*,#1977,.T.);
#2553=ORIENTED_EDGE('',*,*,#1978,.T.);
#2554=ORIENTED_EDGE('',*,*,#1977,.F.);
#2555=ORIENTED_EDGE('',*,*,#1978,.F.);
#2556=ORIENTED_EDGE('',*,*,#1979,.F.);
#2557=ORIENTED_EDGE('',*,*,#1980,.T.);
#2558=ORIENTED_EDGE('',*,*,#1981,.F.);
#2559=ORIENTED_EDGE('',*,*,#1980,.F.);
#2560=ORIENTED_EDGE('',*,*,#1976,.T.);
#2561=ORIENTED_EDGE('',*,*,#1982,.T.);
#2562=ORIENTED_EDGE('',*,*,#1979,.T.);
#2563=ORIENTED_EDGE('',*,*,#1982,.F.);
#2564=ORIENTED_EDGE('',*,*,#1983,.F.);
#2565=ORIENTED_EDGE('',*,*,#1984,.T.);
#2566=ORIENTED_EDGE('',*,*,#1985,.F.);
#2567=ORIENTED_EDGE('',*,*,#1986,.F.);
#2568=ORIENTED_EDGE('',*,*,#1987,.F.);
#2569=ORIENTED_EDGE('',*,*,#1988,.F.);
#2570=ORIENTED_EDGE('',*,*,#1989,.F.);
#2571=ORIENTED_EDGE('',*,*,#1990,.F.);
#2572=ORIENTED_EDGE('',*,*,#1984,.F.);
#2573=ORIENTED_EDGE('',*,*,#1989,.T.);
#2574=ORIENTED_EDGE('',*,*,#1991,.F.);
#2575=ORIENTED_EDGE('',*,*,#1992,.T.);
#2576=ORIENTED_EDGE('',*,*,#1993,.T.);
#2577=ORIENTED_EDGE('',*,*,#1988,.T.);
#2578=ORIENTED_EDGE('',*,*,#1994,.F.);
#2579=ORIENTED_EDGE('',*,*,#1995,.T.);
#2580=ORIENTED_EDGE('',*,*,#1991,.T.);
#2581=ORIENTED_EDGE('',*,*,#1987,.T.);
#2582=ORIENTED_EDGE('',*,*,#1996,.F.);
#2583=ORIENTED_EDGE('',*,*,#1997,.T.);
#2584=ORIENTED_EDGE('',*,*,#1994,.T.);
#2585=ORIENTED_EDGE('',*,*,#1986,.T.);
#2586=ORIENTED_EDGE('',*,*,#1998,.F.);
#2587=ORIENTED_EDGE('',*,*,#1999,.T.);
#2588=ORIENTED_EDGE('',*,*,#1996,.T.);
#2589=ORIENTED_EDGE('',*,*,#1985,.T.);
#2590=ORIENTED_EDGE('',*,*,#2000,.F.);
#2591=ORIENTED_EDGE('',*,*,#2001,.T.);
#2592=ORIENTED_EDGE('',*,*,#1998,.T.);
#2593=ORIENTED_EDGE('',*,*,#1990,.T.);
#2594=ORIENTED_EDGE('',*,*,#1993,.F.);
#2595=ORIENTED_EDGE('',*,*,#2002,.T.);
#2596=ORIENTED_EDGE('',*,*,#2000,.T.);
#2597=ORIENTED_EDGE('',*,*,#1983,.T.);
#2598=ORIENTED_EDGE('',*,*,#1997,.F.);
#2599=ORIENTED_EDGE('',*,*,#1999,.F.);
#2600=ORIENTED_EDGE('',*,*,#2001,.F.);
#2601=ORIENTED_EDGE('',*,*,#2002,.F.);
#2602=ORIENTED_EDGE('',*,*,#1992,.F.);
#2603=ORIENTED_EDGE('',*,*,#1995,.F.);
#2604=ORIENTED_EDGE('',*,*,#1981,.T.);
#3117=CYLINDRICAL_SURFACE('',#3540,0.300000000000034);
#3118=CYLINDRICAL_SURFACE('',#3543,0.294200000000034);
#3209=ADVANCED_FACE('',(#587,#377),#445,.T.);
#3210=ADVANCED_FACE('',(#588),#3117,.T.);
#3211=ADVANCED_FACE('',(#589),#446,.F.);
#3212=ADVANCED_FACE('',(#590),#3118,.T.);
#3213=ADVANCED_FACE('',(#591),#283,.T.);
#3214=ADVANCED_FACE('',(#592),#284,.T.);
#3215=ADVANCED_FACE('',(#593),#447,.T.);
#3216=ADVANCED_FACE('',(#594),#448,.T.);
#3217=ADVANCED_FACE('',(#595),#449,.T.);
#3218=ADVANCED_FACE('',(#596),#450,.T.);
#3219=ADVANCED_FACE('',(#597),#451,.T.);
#3220=ADVANCED_FACE('',(#598),#452,.T.);
#3221=ADVANCED_FACE('',(#599),#453,.T.);
#3222=ADVANCED_FACE('',(#600,#378),#454,.F.);
#3334=CLOSED_SHELL('',(#3209,#3210,#3211,#3212,#3213,#3214,#3215,#3216,
#3217,#3218,#3219,#3220,#3221,#3222));
#3536=AXIS2_PLACEMENT_3D('',#5166,#4144,#4145);
#3537=AXIS2_PLACEMENT_3D('',#5167,#4146,#4147);
#3538=AXIS2_PLACEMENT_3D('',#5169,#4148,#4149);
#3539=AXIS2_PLACEMENT_3D('',#5171,#4150,#4151);
#3540=AXIS2_PLACEMENT_3D('',#5172,#4152,#4153);
#3541=AXIS2_PLACEMENT_3D('',#5175,#4155,#4156);
#3542=AXIS2_PLACEMENT_3D('',#5176,#4157,#4158);
#3543=AXIS2_PLACEMENT_3D('',#5177,#4159,#4160);
#3544=AXIS2_PLACEMENT_3D('',#5179,#4161,#4162);
#3545=AXIS2_PLACEMENT_3D('',#5182,#4164,#4165);
#3546=AXIS2_PLACEMENT_3D('',#5183,#4166,#4167);
#3547=AXIS2_PLACEMENT_3D('',#5185,#4169,#4170);
#3548=AXIS2_PLACEMENT_3D('',#5187,#4171,#4172);
#3549=AXIS2_PLACEMENT_3D('',#5213,#4174,#4175);
#3550=AXIS2_PLACEMENT_3D('',#5219,#4179,#4180);
#3551=AXIS2_PLACEMENT_3D('',#5223,#4183,#4184);
#3552=AXIS2_PLACEMENT_3D('',#5227,#4187,#4188);
#3553=AXIS2_PLACEMENT_3D('',#5231,#4191,#4192);
#3554=AXIS2_PLACEMENT_3D('',#5235,#4195,#4196);
#3555=AXIS2_PLACEMENT_3D('',#5237,#4198,#4199);
#3556=AXIS2_PLACEMENT_3D('',#5238,#4200,#4201);
#4144=DIRECTION('axis',(0.,0.,1.));
#4145=DIRECTION('refdir',(1.,0.,0.));
#4146=DIRECTION('center_axis',(-6.12323399573548E-17,1.,4.78224871431377E-30));
#4147=DIRECTION('ref_axis',(0.939692587475203,5.75395759716863E-17,0.342020234846066));
#4148=DIRECTION('center_axis',(-6.12323399573548E-17,1.,4.78224871431377E-30));
#4149=DIRECTION('ref_axis',(0.939692587475203,5.75395759716863E-17,0.342020234846066));
#4150=DIRECTION('center_axis',(-6.12323399573548E-17,1.,4.78224871431377E-30));
#4151=DIRECTION('ref_axis',(0.939692587475203,5.75395759716863E-17,0.342020234846066));
#4152=DIRECTION('center_axis',(-6.12323399573548E-17,1.,4.78224871431377E-30));
#4153=DIRECTION('ref_axis',(0.939692587475203,5.75395759716863E-17,0.342020234846066));
#4154=DIRECTION('',(6.12323399573548E-17,-1.,-4.78224871431377E-30));
#4155=DIRECTION('center_axis',(-6.12323399573548E-17,1.,4.78224871431377E-30));
#4156=DIRECTION('ref_axis',(0.939692587475203,5.75395759716863E-17,0.342020234846066));
#4157=DIRECTION('center_axis',(-6.12323399573548E-17,1.,4.78224871431377E-30));
#4158=DIRECTION('ref_axis',(0.939692587475203,5.75395759716863E-17,0.342020234846066));
#4159=DIRECTION('center_axis',(6.12323399573548E-17,-1.,-4.78224871431377E-30));
#4160=DIRECTION('ref_axis',(0.939692587475203,5.75395759716863E-17,0.342020234846066));
#4161=DIRECTION('center_axis',(-6.12323399573548E-17,1.,4.78224871431377E-30));
#4162=DIRECTION('ref_axis',(0.939692587475203,5.75395759716863E-17,0.342020234846066));
#4163=DIRECTION('',(-6.12323399573548E-17,1.,4.78224871431377E-30));
#4164=DIRECTION('center_axis',(6.12323399573548E-17,-1.,-4.78224871431377E-30));
#4165=DIRECTION('ref_axis',(0.939692587475203,5.75395759716863E-17,0.342020234846066));
#4166=DIRECTION('center_axis',(-6.12323399573548E-17,1.,4.78224871431377E-30));
#4167=DIRECTION('ref_axis',(0.939692587475203,5.75395759716863E-17,0.342020234846066));
#4168=DIRECTION('',(-0.664463000834449,0.707106781186548,-0.241844827362669));
#4169=DIRECTION('center_axis',(6.12323399573548E-17,-1.,-4.78224871431377E-30));
#4170=DIRECTION('ref_axis',(0.939692587475203,5.75395759716863E-17,0.342020234846066));
#4171=DIRECTION('center_axis',(-6.12323399573548E-17,1.,4.78224871431377E-30));
#4172=DIRECTION('ref_axis',(0.939692587475203,5.75395759716863E-17,0.342020234846066));
#4173=DIRECTION('',(-0.813797652501456,-0.5,-0.296198211985013));
#4174=DIRECTION('center_axis',(0.342020234846066,2.09426992923931E-17,-0.939692587475203));
#4175=DIRECTION('ref_axis',(-0.939692587475203,-5.75395759716863E-17,-0.342020234846066));
#4176=DIRECTION('',(-6.12323399573548E-17,1.,4.78224871431377E-30));
#4177=DIRECTION('',(-0.939692587475203,-5.75395759716863E-17,-0.342020234846066));
#4178=DIRECTION('',(-6.12323399573548E-17,1.,4.78224871431377E-30));
#4179=DIRECTION('center_axis',(0.98480776992449,6.03020841606616E-17,-0.173648081752589));
#4180=DIRECTION('ref_axis',(-0.173648081752589,-1.06328783748123E-17,-0.98480776992449));
#4181=DIRECTION('',(-6.12323399573548E-17,1.,4.78224871431377E-30));
#4182=DIRECTION('',(-0.173648081752589,-1.06328783748123E-17,-0.98480776992449));
#4183=DIRECTION('center_axis',(0.642787535078424,3.93593848682685E-17,0.766044505722614));
#4184=DIRECTION('ref_axis',(0.766044505722614,4.6906697596874E-17,-0.642787535078424));
#4185=DIRECTION('',(-6.12323399573548E-17,1.,4.78224871431377E-30));
#4186=DIRECTION('',(0.766044505722614,4.6906697596874E-17,-0.642787535078424));
#4187=DIRECTION('center_axis',(-0.342020234846066,-2.09426992923931E-17,
0.939692587475203));
#4188=DIRECTION('ref_axis',(0.939692587475203,5.75395759716863E-17,0.342020234846066));
#4189=DIRECTION('',(-6.12323399573548E-17,1.,4.78224871431377E-30));
#4190=DIRECTION('',(0.939692587475203,5.75395759716863E-17,0.342020234846066));
#4191=DIRECTION('center_axis',(-0.98480776992449,-6.03020841606616E-17,
0.173648081752588));
#4192=DIRECTION('ref_axis',(0.173648081752588,1.06328783748123E-17,0.98480776992449));
#4193=DIRECTION('',(-6.12323399573548E-17,1.,4.78224871431377E-30));
#4194=DIRECTION('',(0.173648081752588,1.06328783748123E-17,0.98480776992449));
#4195=DIRECTION('center_axis',(-0.642787535078423,-3.93593848682685E-17,
-0.766044505722615));
#4196=DIRECTION('ref_axis',(-0.766044505722615,-4.6906697596874E-17,0.642787535078423));
#4197=DIRECTION('',(-0.766044505722615,-4.6906697596874E-17,0.642787535078423));
#4198=DIRECTION('center_axis',(-6.12323399573548E-17,1.,4.78224871431377E-30));
#4199=DIRECTION('ref_axis',(-0.342020234846066,-2.09426992923931E-17,0.939692587475203));
#4200=DIRECTION('center_axis',(-6.12323399573548E-17,1.,4.78224871431377E-30));
#4201=DIRECTION('ref_axis',(0.939692587475203,5.75395759716863E-17,0.342020234846066));
#5166=CARTESIAN_POINT('',(0.,0.,0.));
#5167=CARTESIAN_POINT('Origin',(2.34923146868827,-1.27000000000034,3.85505058711526));
#5168=CARTESIAN_POINT('',(2.06732369244568,-1.27000000000034,3.75244451666143));
#5169=CARTESIAN_POINT('Origin',(2.34923146868827,-1.27000000000034,3.85505058711526));
#5170=CARTESIAN_POINT('',(2.11430832181945,-1.27000000000034,3.76954552840374));
#5171=CARTESIAN_POINT('Origin',(2.34923146868827,-1.27000000000034,3.85505058711526));
#5172=CARTESIAN_POINT('Origin',(2.34923146868828,-2.28000000000046,3.85505058711526));
#5173=CARTESIAN_POINT('',(2.06732369244568,-2.28000000000046,3.75244451666143));
#5174=CARTESIAN_POINT('',(2.06732369244568,-2.28000000000046,3.75244451666143));
#5175=CARTESIAN_POINT('Origin',(2.34923146868828,-2.28000000000046,3.85505058711526));
#5176=CARTESIAN_POINT('Origin',(2.34923146868828,-2.28000000000046,3.85505058711526));
#5177=CARTESIAN_POINT('Origin',(2.34923146868827,0.274999999999834,3.85505058711526));
#5178=CARTESIAN_POINT('',(2.07277390945304,-1.22580000000034,3.75442823402354));
#5179=CARTESIAN_POINT('Origin',(2.34923146868827,-1.22580000000034,3.85505058711526));
#5180=CARTESIAN_POINT('',(2.07277390945304,1.72,3.75442823402354));
#5181=CARTESIAN_POINT('',(2.07277390945304,0.274999999999834,3.75442823402354));
#5182=CARTESIAN_POINT('Origin',(2.34923146868827,1.72,3.85505058711526));
#5183=CARTESIAN_POINT('Origin',(2.34923146868827,-1.25000000000034,3.85505058711526));
#5184=CARTESIAN_POINT('',(2.09551447006994,-1.25000000000034,3.76270512370681));
#5185=CARTESIAN_POINT('Origin',(2.34923146868827,2.06158650880643,3.85505058711526));
#5186=CARTESIAN_POINT('',(1.9028774896375,2.12000000000004,3.69259097556336));
#5187=CARTESIAN_POINT('Origin',(2.34923146868827,2.12000000000004,3.85505058711526));
#5188=CARTESIAN_POINT('',(1.80669970035391,2.06090804453178,3.65758511245857));
#5189=CARTESIAN_POINT('',(1.80780396562194,2.06158650880643,3.65798703226866));
#5190=CARTESIAN_POINT('',(1.90695546709804,2.06090804453178,4.22616414352457));
#5191=CARTESIAN_POINT('Ctrl Pts',(1.90695546709804,2.06090804453178,4.22616414352457));
#5192=CARTESIAN_POINT('Ctrl Pts',(1.8568275837256,2.14424137786374,3.94187462798943));
#5193=CARTESIAN_POINT('Ctrl Pts',(1.80669970035391,2.06090804453178,3.65758511245857));
#5194=CARTESIAN_POINT('',(2.44948723543241,2.06090804453178,4.42362961818127));
#5195=CARTESIAN_POINT('Ctrl Pts',(2.44948723543241,2.06090804453178,4.42362961818127));
#5196=CARTESIAN_POINT('Ctrl Pts',(2.17822135126319,2.14424137786374,4.32489688085218));
#5197=CARTESIAN_POINT('Ctrl Pts',(1.90695546709804,2.06090804453178,4.22616414352457));
#5198=CARTESIAN_POINT('',(2.89176323702264,2.06090804453178,4.05251606177196));
#5199=CARTESIAN_POINT('Ctrl Pts',(2.89176323702264,2.06090804453178,4.05251606177196));
#5200=CARTESIAN_POINT('Ctrl Pts',(2.67062523622586,2.14424137786374,4.23807283997801));
#5201=CARTESIAN_POINT('Ctrl Pts',(2.44948723543241,2.06090804453178,4.42362961818127));
#5202=CARTESIAN_POINT('',(2.79150747027851,2.06090804453178,3.48393703070596));
#5203=CARTESIAN_POINT('Ctrl Pts',(2.79150747027851,2.06090804453178,3.48393703070596));
#5204=CARTESIAN_POINT('Ctrl Pts',(2.84163535365095,2.14424137786374,3.76822654624109));
#5205=CARTESIAN_POINT('Ctrl Pts',(2.89176323702264,2.06090804453178,4.05251606177196));
#5206=CARTESIAN_POINT('',(2.24897570194414,2.06090804453178,3.28647155604926));
#5207=CARTESIAN_POINT('Ctrl Pts',(2.24897570194414,2.06090804453178,3.28647155604926));
#5208=CARTESIAN_POINT('Ctrl Pts',(2.52024158611336,2.14424137786374,3.38520429337835));
#5209=CARTESIAN_POINT('Ctrl Pts',(2.79150747027851,2.06090804453178,3.48393703070596));
#5210=CARTESIAN_POINT('Ctrl Pts',(1.80669970035391,2.06090804453178,3.65758511245857));
#5211=CARTESIAN_POINT('Ctrl Pts',(2.02783770115069,2.14424137786374,3.47202833425252));
#5212=CARTESIAN_POINT('Ctrl Pts',(2.24897570194414,2.06090804453178,3.28647155604926));
#5213=CARTESIAN_POINT('Origin',(2.79150747027851,1.72,3.48393703070596));
#5214=CARTESIAN_POINT('',(2.79150747027851,1.72,3.48393703070596));
#5215=CARTESIAN_POINT('',(2.79150747027851,1.72,3.48393703070596));
#5216=CARTESIAN_POINT('',(2.24897570194414,1.72,3.28647155604926));
#5217=CARTESIAN_POINT('',(2.79150747027851,1.72,3.48393703070596));
#5218=CARTESIAN_POINT('',(2.24897570194414,1.72,3.28647155604926));
#5219=CARTESIAN_POINT('Origin',(2.89176323702264,1.72,4.05251606177196));
#5220=CARTESIAN_POINT('',(2.89176323702264,1.72,4.05251606177196));
#5221=CARTESIAN_POINT('',(2.89176323702264,1.72,4.05251606177196));
#5222=CARTESIAN_POINT('',(2.89176323702264,1.72,4.05251606177196));
#5223=CARTESIAN_POINT('Origin',(2.44948723543241,1.72,4.42362961818127));
#5224=CARTESIAN_POINT('',(2.44948723543241,1.72,4.42362961818127));
#5225=CARTESIAN_POINT('',(2.44948723543241,1.72,4.42362961818127));
#5226=CARTESIAN_POINT('',(2.44948723543241,1.72,4.42362961818127));
#5227=CARTESIAN_POINT('Origin',(1.90695546709804,1.72,4.22616414352457));
#5228=CARTESIAN_POINT('',(1.90695546709804,1.72,4.22616414352457));
#5229=CARTESIAN_POINT('',(1.90695546709804,1.72,4.22616414352457));
#5230=CARTESIAN_POINT('',(1.90695546709804,1.72,4.22616414352457));
#5231=CARTESIAN_POINT('Origin',(1.80669970035391,1.72,3.65758511245857));
#5232=CARTESIAN_POINT('',(1.80669970035391,1.72,3.65758511245857));
#5233=CARTESIAN_POINT('',(1.80669970035391,1.72,3.65758511245857));
#5234=CARTESIAN_POINT('',(1.80669970035391,1.72,3.65758511245857));
#5235=CARTESIAN_POINT('Origin',(2.24897570194414,1.72,3.28647155604926));
#5236=CARTESIAN_POINT('',(2.24897570194414,1.72,3.28647155604926));
#5237=CARTESIAN_POINT('Origin',(2.34923146868827,2.12000000000004,3.85505058711526));
#5238=CARTESIAN_POINT('Origin',(2.34923146868827,1.72,3.85505058711526));
#5888=UNCERTAINTY_MEASURE_WITH_UNIT(LENGTH_MEASURE(0.001),#5930,
'DISTANCE_ACCURACY_VALUE',
'Maximum model space distance between geometric entities at asserted c
onnectivities');
#5905=UNCERTAINTY_MEASURE_WITH_UNIT(LENGTH_MEASURE(0.001),#5930,
'DISTANCE_ACCURACY_VALUE',
'Maximum model space distance between geometric entities at asserted c
onnectivities');
#5912=(
GEOMETRIC_REPRESENTATION_CONTEXT(3)
GLOBAL_UNCERTAINTY_ASSIGNED_CONTEXT((#5888))
GLOBAL_UNIT_ASSIGNED_CONTEXT((#5930,#5932,#5933))
REPRESENTATION_CONTEXT('','3D')
);
#5929=(
GEOMETRIC_REPRESENTATION_CONTEXT(3)
GLOBAL_UNCERTAINTY_ASSIGNED_CONTEXT((#5905))
GLOBAL_UNIT_ASSIGNED_CONTEXT((#5930,#5932,#5933))
REPRESENTATION_CONTEXT('','3D')
);
#5930=(
LENGTH_UNIT()
NAMED_UNIT(*)
SI_UNIT(.CENTI.,.METRE.)
);
#5932=(
NAMED_UNIT(*)
PLANE_ANGLE_UNIT()
SI_UNIT($,.RADIAN.)
);
#5933=(
NAMED_UNIT(*)
SI_UNIT($,.STERADIAN.)
SOLID_ANGLE_UNIT()
);
#5940=SHAPE_DEFINITION_REPRESENTATION(#5963,#6045);
#5963=PRODUCT_DEFINITION_SHAPE('',$,#6069);
#6045=SHAPE_REPRESENTATION('',(#3536),#5912);
#6062=PRODUCT_DEFINITION_CONTEXT('part definition',#6133,'design');
#6069=PRODUCT_DEFINITION('Forty millimetre hinge bolt',
'Forty millimetre hinge bolt',#6092,#6062);
#6092=PRODUCT_DEFINITION_FORMATION('',$,#6141);
#6133=APPLICATION_CONTEXT(
'Core Data for Automotive Mechanical Design Process');
#6134=PRODUCT_CONTEXT('part definition',#6133,'mechanical');
#6141=PRODUCT('Forty millimetre hinge bolt',
'Forty millimetre hinge bolt','Forty millimetre hinge bolt',(#6134));
#6221=COLOUR_RGB('Black',0.12,0.14,0.17);
#6222=FILL_AREA_STYLE_COLOUR('',#6221);
#6223=FILL_AREA_STYLE('',(#6222));
#6224=SURFACE_STYLE_FILL_AREA(#6223);
#6225=SURFACE_SIDE_STYLE('',(#6224));
#6226=SURFACE_STYLE_USAGE(.BOTH.,#6225);
#6227=PRESENTATION_STYLE_ASSIGNMENT((#6226));
ENDSEC;
END-ISO-10303-21;
